ISO-10303-21;
HEADER;
/* Generated by software containing ST-Developer
 * from STEP Tools, Inc. (www.steptools.com) 
 */

FILE_DESCRIPTION(
/* description */ ('Bell-crank linkage with push rods'),
/* implementation_level */ '2;1');

FILE_NAME(
/* name */ 'Vertical lower pin sleeve (1).step',
/* time_stamp */ '2026-10-28T03:25:15-07:00',
/* author */ (''),
/* organization */ (''),
/* preprocessor_version */ 'ST-DEVELOPER v20.2',
/* originating_system */ 'Autodesk Translation Framework v15.17.0.0',
/* authorisation */ '');

FILE_SCHEMA (('AUTOMOTIVE_DESIGN { 1 0 10303 214 3 1 1 }'));
ENDSEC;

DATA;
#10=MECHANICAL_DESIGN_GEOMETRIC_PRESENTATION_REPRESENTATION('',(#660),#16678);
#544=SHAPE_REPRESENTATION_RELATIONSHIP('SRR','None',#16966,#598);
#598=ADVANCED_BREP_SHAPE_REPRESENTATION('',(#720),#16671);
#660=STYLED_ITEM('',(#17291),#720);
#720=MANIFOLD_SOLID_BREP('Body1',#8852);
#948=FACE_BOUND('',#2464,.T.);
#949=FACE_BOUND('',#2466,.T.);
#1213=PLANE('',#10446);
#1214=PLANE('',#10447);
#1716=FACE_OUTER_BOUND('',#2461,.T.);
#1717=FACE_OUTER_BOUND('',#2462,.T.);
#1718=FACE_OUTER_BOUND('',#2463,.T.);
#1719=FACE_OUTER_BOUND('',#2465,.T.);
#2461=EDGE_LOOP('',(#7875,#7876,#7877,#7878));
#2462=EDGE_LOOP('',(#7879,#7880,#7881,#7882));
#2463=EDGE_LOOP('',(#7883));
#2464=EDGE_LOOP('',(#7884));
#2465=EDGE_LOOP('',(#7885));
#2466=EDGE_LOOP('',(#7886));
#3026=LINE('',#16247,#3575);
#3027=LINE('',#16253,#3576);
#3575=VECTOR('',#13100,0.305);
#3576=VECTOR('',#13107,0.5);
#4079=CIRCLE('',#10441,0.305);
#4080=CIRCLE('',#10442,0.305);
#4081=CIRCLE('',#10444,0.5);
#4082=CIRCLE('',#10445,0.5);
#4770=VERTEX_POINT('',#16244);
#4771=VERTEX_POINT('',#16246);
#4772=VERTEX_POINT('',#16250);
#4773=VERTEX_POINT('',#16252);
#5815=EDGE_CURVE('',#4770,#4770,#4079,.T.);
#5816=EDGE_CURVE('',#4770,#4771,#3026,.T.);
#5817=EDGE_CURVE('',#4771,#4771,#4080,.T.);
#5818=EDGE_CURVE('',#4772,#4772,#4081,.T.);
#5819=EDGE_CURVE('',#4772,#4773,#3027,.T.);
#5820=EDGE_CURVE('',#4773,#4773,#4082,.T.);
#7875=ORIENTED_EDGE('',*,*,#5815,.F.);
#7876=ORIENTED_EDGE('',*,*,#5816,.T.);
#7877=ORIENTED_EDGE('',*,*,#5817,.T.);
#7878=ORIENTED_EDGE('',*,*,#5816,.F.);
#7879=ORIENTED_EDGE('',*,*,#5818,.F.);
#7880=ORIENTED_EDGE('',*,*,#5819,.T.);
#7881=ORIENTED_EDGE('',*,*,#5820,.T.);
#7882=ORIENTED_EDGE('',*,*,#5819,.F.);
#7883=ORIENTED_EDGE('',*,*,#5818,.T.);
#7884=ORIENTED_EDGE('',*,*,#5815,.T.);
#7885=ORIENTED_EDGE('',*,*,#5820,.F.);
#7886=ORIENTED_EDGE('',*,*,#5817,.F.);
#8256=CYLINDRICAL_SURFACE('',#10440,0.305);
#8257=CYLINDRICAL_SURFACE('',#10443,0.5);
#8741=ADVANCED_FACE('',(#1716),#8256,.F.);
#8742=ADVANCED_FACE('',(#1717),#8257,.T.);
#8743=ADVANCED_FACE('',(#1718,#948),#1213,.T.);
#8744=ADVANCED_FACE('',(#1719,#949),#1214,.F.);
#8852=CLOSED_SHELL('',(#8741,#8742,#8743,#8744));
#10439=AXIS2_PLACEMENT_3D('',#16242,#13094,#13095);
#10440=AXIS2_PLACEMENT_3D('',#16243,#13096,#13097);
#10441=AXIS2_PLACEMENT_3D('',#16245,#13098,#13099);
#10442=AXIS2_PLACEMENT_3D('',#16248,#13101,#13102);
#10443=AXIS2_PLACEMENT_3D('',#16249,#13103,#13104);
#10444=AXIS2_PLACEMENT_3D('',#16251,#13105,#13106);
#10445=AXIS2_PLACEMENT_3D('',#16254,#13108,#13109);
#10446=AXIS2_PLACEMENT_3D('',#16255,#13110,#13111);
#10447=AXIS2_PLACEMENT_3D('',#16256,#13112,#13113);
#13094=DIRECTION('axis',(0.,0.,1.));
#13095=DIRECTION('refdir',(1.,0.,0.));
#13096=DIRECTION('center_axis',(0.,0.,1.));
#13097=DIRECTION('ref_axis',(1.,0.,0.));
#13098=DIRECTION('center_axis',(0.,0.,-1.));
#13099=DIRECTION('ref_axis',(1.,0.,0.));
#13100=DIRECTION('',(0.,0.,-1.));
#13101=DIRECTION('center_axis',(0.,0.,-1.));
#13102=DIRECTION('ref_axis',(1.,0.,0.));
#13103=DIRECTION('center_axis',(0.,0.,1.));
#13104=DIRECTION('ref_axis',(1.,0.,0.));
#13105=DIRECTION('center_axis',(0.,0.,1.));
#13106=DIRECTION('ref_axis',(1.,0.,0.));
#13107=DIRECTION('',(0.,0.,-1.));
#13108=DIRECTION('center_axis',(0.,0.,1.));
#13109=DIRECTION('ref_axis',(1.,0.,0.));
#13110=DIRECTION('center_axis',(0.,0.,1.));
#13111=DIRECTION('ref_axis',(1.,0.,0.));
#13112=DIRECTION('center_axis',(0.,0.,1.));
#13113=DIRECTION('ref_axis',(1.,0.,0.));
#16242=CARTESIAN_POINT('',(0.,0.,0.));
#16243=CARTESIAN_POINT('Origin',(4.,12.,6.1));
#16244=CARTESIAN_POINT('',(3.695,12.,6.8));
#16245=CARTESIAN_POINT('Origin',(4.,12.,6.8));
#16246=CARTESIAN_POINT('',(3.695,12.,6.1));
#16247=CARTESIAN_POINT('',(3.695,12.,6.1));
#16248=CARTESIAN_POINT('Origin',(4.,12.,6.1));
#16249=CARTESIAN_POINT('Origin',(4.,12.,6.1));
#16250=CARTESIAN_POINT('',(3.5,12.,6.8));
#16251=CARTESIAN_POINT('Origin',(4.,12.,6.8));
#16252=CARTESIAN_POINT('',(3.5,12.,6.1));
#16253=CARTESIAN_POINT('',(3.5,12.,6.1));
#16254=CARTESIAN_POINT('Origin',(4.,12.,6.1));
#16255=CARTESIAN_POINT('Origin',(4.,12.,6.8));
#16256=CARTESIAN_POINT('Origin',(4.,12.,6.1));
#16607=UNCERTAINTY_MEASURE_WITH_UNIT(LENGTH_MEASURE(0.001),#16679,
'DISTANCE_ACCURACY_VALUE',
'Maximum model space distance between geometric entities at asserted c
onnectivities');
#16614=UNCERTAINTY_MEASURE_WITH_UNIT(LENGTH_MEASURE(0.001),#16679,
'DISTANCE_ACCURACY_VALUE',
'Maximum model space distance between geometric entities at asserted c
onnectivities');
#16671=(
GEOMETRIC_REPRESENTATION_CONTEXT(3)
GLOBAL_UNCERTAINTY_ASSIGNED_CONTEXT((#16607))
GLOBAL_UNIT_ASSIGNED_CONTEXT((#16679,#16681,#16682))
REPRESENTATION_CONTEXT('','3D')
);
#16678=(
GEOMETRIC_REPRESENTATION_CONTEXT(3)
GLOBAL_UNCERTAINTY_ASSIGNED_CONTEXT((#16614))
GLOBAL_UNIT_ASSIGNED_CONTEXT((#16679,#16681,#16682))
REPRESENTATION_CONTEXT('','3D')
);
#16679=(
LENGTH_UNIT()
NAMED_UNIT(*)
SI_UNIT(.CENTI.,.METRE.)
);
#16681=(
NAMED_UNIT(*)
PLANE_ANGLE_UNIT()
SI_UNIT($,.RADIAN.)
);
#16682=(
NAMED_UNIT(*)
SI_UNIT($,.STERADIAN.)
SOLID_ANGLE_UNIT()
);
#16739=SHAPE_DEFINITION_REPRESENTATION(#16813,#16966);
#16813=PRODUCT_DEFINITION_SHAPE('',$,#17030);
#16966=SHAPE_REPRESENTATION('',(#10439),#16671);
#16973=PRODUCT_DEFINITION_CONTEXT('part definition',#17164,'design');
#17030=PRODUCT_DEFINITION('Vertical lower pin sleeve (1)',
'Vertical lower pin sleeve (1)',#17093,#16973);
#17093=PRODUCT_DEFINITION_FORMATION('',$,#17222);
#17164=APPLICATION_CONTEXT(
'Core Data for Automotive Mechanical Design Process');
#17165=PRODUCT_CONTEXT('part definition',#17164,'mechanical');
#17222=PRODUCT('Vertical lower pin sleeve (1)',
'Vertical lower pin sleeve (1)','Vertical lower pin sleeve (1)',(#17165));
#17285=COLOUR_RGB('Grey',0.48,0.52,0.57);
#17286=FILL_AREA_STYLE_COLOUR('',#17285);
#17287=FILL_AREA_STYLE('',(#17286));
#17288=SURFACE_STYLE_FILL_AREA(#17287);
#17289=SURFACE_SIDE_STYLE('',(#17288));
#17290=SURFACE_STYLE_USAGE(.BOTH.,#17289);
#17291=PRESENTATION_STYLE_ASSIGNMENT((#17290));
ENDSEC;
END-ISO-10303-21;
